ISO-10303-21;
HEADER;
/* Generated by software containing ST-Developer
 * from STEP Tools, Inc. (www.steptools.com) 
 */

FILE_DESCRIPTION(
/* description */ ('Caster wheel assembly'),
/* implementation_level */ '2;1');

FILE_NAME(
/* name */ 'M4x10 Cap Screw.step',
/* time_stamp */ '2026-10-28T03:23:56-07:00',
/* author */ (''),
/* organization */ (''),
/* preprocessor_version */ 'ST-DEVELOPER v20.2',
/* originating_system */ 'Autodesk Translation Framework v15.17.0.0',
/* authorisation */ '');

FILE_SCHEMA (('AUTOMOTIVE_DESIGN { 1 0 10303 214 3 1 1 }'));
ENDSEC;

DATA;
#10=MECHANICAL_DESIGN_GEOMETRIC_PRESENTATION_REPRESENTATION('',(#235),#5385);
#47=ORIENTED_CLOSED_SHELL('',*,#2662,.F.);
#48=BREP_WITH_VOIDS('Body1',#2663,(#47));
#171=CONICAL_SURFACE('',#3106,0.325,0.785398163397448);
#172=CONICAL_SURFACE('',#3110,0.335,0.785398163397448);
#173=CONICAL_SURFACE('',#3114,0.21,0.463647609000806);
#191=SHAPE_REPRESENTATION_RELATIONSHIP('SRR','None',#5487,#213);
#213=ADVANCED_BREP_SHAPE_REPRESENTATION('',(#48),#5374);
#235=STYLED_ITEM('',(#5679),#48);
#315=FACE_BOUND('',#722,.T.);
#385=PLANE('',#3094);
#386=PLANE('',#3095);
#387=PLANE('',#3096);
#388=PLANE('',#3097);
#389=PLANE('',#3098);
#390=PLANE('',#3099);
#391=PLANE('',#3100);
#392=PLANE('',#3101);
#393=PLANE('',#3102);
#394=PLANE('',#3104);
#395=PLANE('',#3112);
#506=FACE_OUTER_BOUND('',#708,.T.);
#507=FACE_OUTER_BOUND('',#709,.T.);
#508=FACE_OUTER_BOUND('',#710,.T.);
#509=FACE_OUTER_BOUND('',#711,.T.);
#510=FACE_OUTER_BOUND('',#712,.T.);
#511=FACE_OUTER_BOUND('',#713,.T.);
#512=FACE_OUTER_BOUND('',#714,.T.);
#513=FACE_OUTER_BOUND('',#715,.T.);
#514=FACE_OUTER_BOUND('',#716,.T.);
#515=FACE_OUTER_BOUND('',#717,.T.);
#516=FACE_OUTER_BOUND('',#718,.T.);
#517=FACE_OUTER_BOUND('',#719,.T.);
#518=FACE_OUTER_BOUND('',#720,.T.);
#519=FACE_OUTER_BOUND('',#721,.T.);
#520=FACE_OUTER_BOUND('',#723,.T.);
#521=FACE_OUTER_BOUND('',#724,.T.);
#708=EDGE_LOOP('',(#2108,#2109,#2110,#2111));
#709=EDGE_LOOP('',(#2112,#2113,#2114,#2115));
#710=EDGE_LOOP('',(#2116,#2117,#2118,#2119));
#711=EDGE_LOOP('',(#2120,#2121,#2122,#2123));
#712=EDGE_LOOP('',(#2124,#2125,#2126,#2127));
#713=EDGE_LOOP('',(#2128,#2129,#2130,#2131));
#714=EDGE_LOOP('',(#2132,#2133,#2134,#2135,#2136,#2137));
#715=EDGE_LOOP('',(#2138,#2139,#2140,#2141,#2142,#2143));
#716=EDGE_LOOP('',(#2144));
#717=EDGE_LOOP('',(#2145));
#718=EDGE_LOOP('',(#2146,#2147,#2148,#2149));
#719=EDGE_LOOP('',(#2150,#2151,#2152,#2153));
#720=EDGE_LOOP('',(#2154,#2155,#2156,#2157));
#721=EDGE_LOOP('',(#2158));
#722=EDGE_LOOP('',(#2159));
#723=EDGE_LOOP('',(#2160,#2161,#2162,#2163));
#724=EDGE_LOOP('',(#2164,#2165,#2166,#2167));
#896=LINE('',#4605,#1030);
#897=LINE('',#4607,#1031);
#898=LINE('',#4609,#1032);
#899=LINE('',#4610,#1033);
#900=LINE('',#4613,#1034);
#901=LINE('',#4615,#1035);
#902=LINE('',#4616,#1036);
#903=LINE('',#4619,#1037);
#904=LINE('',#4621,#1038);
#905=LINE('',#4622,#1039);
#906=LINE('',#4625,#1040);
#907=LINE('',#4627,#1041);
#908=LINE('',#4628,#1042);
#909=LINE('',#4631,#1043);
#910=LINE('',#4633,#1044);
#911=LINE('',#4634,#1045);
#912=LINE('',#4636,#1046);
#913=LINE('',#4637,#1047);
#914=LINE('',#4649,#1048);
#915=LINE('',#4653,#1049);
#916=LINE('',#4657,#1050);
#917=LINE('',#4664,#1051);
#918=LINE('',#4666,#1052);
#1030=VECTOR('',#3735,1.);
#1031=VECTOR('',#3736,1.);
#1032=VECTOR('',#3737,1.);
#1033=VECTOR('',#3738,1.);
#1034=VECTOR('',#3741,1.);
#1035=VECTOR('',#3742,1.);
#1036=VECTOR('',#3743,1.);
#1037=VECTOR('',#3746,1.);
#1038=VECTOR('',#3747,1.);
#1039=VECTOR('',#3748,1.);
#1040=VECTOR('',#3751,1.);
#1041=VECTOR('',#3752,1.);
#1042=VECTOR('',#3753,1.);
#1043=VECTOR('',#3756,1.);
#1044=VECTOR('',#3757,1.);
#1045=VECTOR('',#3758,1.);
#1046=VECTOR('',#3761,1.);
#1047=VECTOR('',#3762,1.);
#1048=VECTOR('',#3779,0.325);
#1049=VECTOR('',#3784,0.35);
#1050=VECTOR('',#3789,0.335);
#1051=VECTOR('',#3798,0.21);
#1052=VECTOR('',#3801,0.2);
#1141=CIRCLE('',#3103,0.1954);
#1142=CIRCLE('',#3105,0.3);
#1143=CIRCLE('',#3107,0.35);
#1144=CIRCLE('',#3109,0.35);
#1145=CIRCLE('',#3111,0.32);
#1146=CIRCLE('',#3113,0.22);
#1147=CIRCLE('',#3115,0.1954);
#1344=VERTEX_POINT('',#4603);
#1345=VERTEX_POINT('',#4604);
#1346=VERTEX_POINT('',#4606);
#1347=VERTEX_POINT('',#4608);
#1348=VERTEX_POINT('',#4612);
#1349=VERTEX_POINT('',#4614);
#1350=VERTEX_POINT('',#4618);
#1351=VERTEX_POINT('',#4620);
#1352=VERTEX_POINT('',#4624);
#1353=VERTEX_POINT('',#4626);
#1354=VERTEX_POINT('',#4630);
#1355=VERTEX_POINT('',#4632);
#1356=VERTEX_POINT('',#4641);
#1357=VERTEX_POINT('',#4644);
#1358=VERTEX_POINT('',#4647);
#1359=VERTEX_POINT('',#4651);
#1360=VERTEX_POINT('',#4655);
#1361=VERTEX_POINT('',#4659);
#1362=VERTEX_POINT('',#4662);
#1622=EDGE_CURVE('',#1344,#1345,#896,.T.);
#1623=EDGE_CURVE('',#1345,#1346,#897,.T.);
#1624=EDGE_CURVE('',#1346,#1347,#898,.T.);
#1625=EDGE_CURVE('',#1344,#1347,#899,.T.);
#1626=EDGE_CURVE('',#1345,#1348,#900,.T.);
#1627=EDGE_CURVE('',#1348,#1349,#901,.T.);
#1628=EDGE_CURVE('',#1349,#1346,#902,.T.);
#1629=EDGE_CURVE('',#1348,#1350,#903,.T.);
#1630=EDGE_CURVE('',#1350,#1351,#904,.T.);
#1631=EDGE_CURVE('',#1351,#1349,#905,.T.);
#1632=EDGE_CURVE('',#1350,#1352,#906,.T.);
#1633=EDGE_CURVE('',#1352,#1353,#907,.T.);
#1634=EDGE_CURVE('',#1353,#1351,#908,.T.);
#1635=EDGE_CURVE('',#1352,#1354,#909,.T.);
#1636=EDGE_CURVE('',#1354,#1355,#910,.T.);
#1637=EDGE_CURVE('',#1355,#1353,#911,.T.);
#1638=EDGE_CURVE('',#1354,#1344,#912,.T.);
#1639=EDGE_CURVE('',#1347,#1355,#913,.T.);
#1640=EDGE_CURVE('',#1356,#1356,#1141,.T.);
#1641=EDGE_CURVE('',#1357,#1357,#1142,.T.);
#1642=EDGE_CURVE('',#1358,#1358,#1143,.T.);
#1643=EDGE_CURVE('',#1358,#1357,#914,.T.);
#1644=EDGE_CURVE('',#1359,#1359,#1144,.T.);
#1645=EDGE_CURVE('',#1359,#1358,#915,.T.);
#1646=EDGE_CURVE('',#1360,#1360,#1145,.T.);
#1647=EDGE_CURVE('',#1360,#1359,#916,.T.);
#1648=EDGE_CURVE('',#1361,#1361,#1146,.T.);
#1649=EDGE_CURVE('',#1362,#1362,#1147,.F.);
#1650=EDGE_CURVE('',#1362,#1361,#917,.T.);
#1651=EDGE_CURVE('',#1356,#1362,#918,.T.);
#2108=ORIENTED_EDGE('',*,*,#1622,.T.);
#2109=ORIENTED_EDGE('',*,*,#1623,.T.);
#2110=ORIENTED_EDGE('',*,*,#1624,.T.);
#2111=ORIENTED_EDGE('',*,*,#1625,.F.);
#2112=ORIENTED_EDGE('',*,*,#1626,.T.);
#2113=ORIENTED_EDGE('',*,*,#1627,.T.);
#2114=ORIENTED_EDGE('',*,*,#1628,.T.);
#2115=ORIENTED_EDGE('',*,*,#1623,.F.);
#2116=ORIENTED_EDGE('',*,*,#1629,.T.);
#2117=ORIENTED_EDGE('',*,*,#1630,.T.);
#2118=ORIENTED_EDGE('',*,*,#1631,.T.);
#2119=ORIENTED_EDGE('',*,*,#1627,.F.);
#2120=ORIENTED_EDGE('',*,*,#1632,.T.);
#2121=ORIENTED_EDGE('',*,*,#1633,.T.);
#2122=ORIENTED_EDGE('',*,*,#1634,.T.);
#2123=ORIENTED_EDGE('',*,*,#1630,.F.);
#2124=ORIENTED_EDGE('',*,*,#1635,.T.);
#2125=ORIENTED_EDGE('',*,*,#1636,.T.);
#2126=ORIENTED_EDGE('',*,*,#1637,.T.);
#2127=ORIENTED_EDGE('',*,*,#1633,.F.);
#2128=ORIENTED_EDGE('',*,*,#1638,.T.);
#2129=ORIENTED_EDGE('',*,*,#1625,.T.);
#2130=ORIENTED_EDGE('',*,*,#1639,.T.);
#2131=ORIENTED_EDGE('',*,*,#1636,.F.);
#2132=ORIENTED_EDGE('',*,*,#1638,.F.);
#2133=ORIENTED_EDGE('',*,*,#1635,.F.);
#2134=ORIENTED_EDGE('',*,*,#1632,.F.);
#2135=ORIENTED_EDGE('',*,*,#1629,.F.);
#2136=ORIENTED_EDGE('',*,*,#1626,.F.);
#2137=ORIENTED_EDGE('',*,*,#1622,.F.);
#2138=ORIENTED_EDGE('',*,*,#1639,.F.);
#2139=ORIENTED_EDGE('',*,*,#1624,.F.);
#2140=ORIENTED_EDGE('',*,*,#1628,.F.);
#2141=ORIENTED_EDGE('',*,*,#1631,.F.);
#2142=ORIENTED_EDGE('',*,*,#1634,.F.);
#2143=ORIENTED_EDGE('',*,*,#1637,.F.);
#2144=ORIENTED_EDGE('',*,*,#1640,.F.);
#2145=ORIENTED_EDGE('',*,*,#1641,.F.);
#2146=ORIENTED_EDGE('',*,*,#1642,.F.);
#2147=ORIENTED_EDGE('',*,*,#1643,.T.);
#2148=ORIENTED_EDGE('',*,*,#1641,.T.);
#2149=ORIENTED_EDGE('',*,*,#1643,.F.);
#2150=ORIENTED_EDGE('',*,*,#1644,.F.);
#2151=ORIENTED_EDGE('',*,*,#1645,.T.);
#2152=ORIENTED_EDGE('',*,*,#1642,.T.);
#2153=ORIENTED_EDGE('',*,*,#1645,.F.);
#2154=ORIENTED_EDGE('',*,*,#1646,.F.);
#2155=ORIENTED_EDGE('',*,*,#1647,.T.);
#2156=ORIENTED_EDGE('',*,*,#1644,.T.);
#2157=ORIENTED_EDGE('',*,*,#1647,.F.);
#2158=ORIENTED_EDGE('',*,*,#1646,.T.);
#2159=ORIENTED_EDGE('',*,*,#1648,.F.);
#2160=ORIENTED_EDGE('',*,*,#1649,.F.);
#2161=ORIENTED_EDGE('',*,*,#1650,.T.);
#2162=ORIENTED_EDGE('',*,*,#1648,.T.);
#2163=ORIENTED_EDGE('',*,*,#1650,.F.);
#2164=ORIENTED_EDGE('',*,*,#1640,.T.);
#2165=ORIENTED_EDGE('',*,*,#1651,.T.);
#2166=ORIENTED_EDGE('',*,*,#1649,.T.);
#2167=ORIENTED_EDGE('',*,*,#1651,.F.);
#2459=CYLINDRICAL_SURFACE('',#3108,0.35);
#2460=CYLINDRICAL_SURFACE('',#3116,0.1954);
#2566=ADVANCED_FACE('',(#506),#385,.F.);
#2567=ADVANCED_FACE('',(#507),#386,.F.);
#2568=ADVANCED_FACE('',(#508),#387,.F.);
#2569=ADVANCED_FACE('',(#509),#388,.F.);
#2570=ADVANCED_FACE('',(#510),#389,.F.);
#2571=ADVANCED_FACE('',(#511),#390,.F.);
#2572=ADVANCED_FACE('',(#512),#391,.F.);
#2573=ADVANCED_FACE('',(#513),#392,.F.);
#2574=ADVANCED_FACE('',(#514),#393,.F.);
#2575=ADVANCED_FACE('',(#515),#394,.T.);
#2576=ADVANCED_FACE('',(#516),#171,.T.);
#2577=ADVANCED_FACE('',(#517),#2459,.T.);
#2578=ADVANCED_FACE('',(#518),#172,.T.);
#2579=ADVANCED_FACE('',(#519,#315),#395,.T.);
#2580=ADVANCED_FACE('',(#520),#173,.T.);
#2581=ADVANCED_FACE('',(#521),#2460,.T.);
#2662=CLOSED_SHELL('',(#2566,#2567,#2568,#2569,#2570,#2571,#2572,#2573));
#2663=CLOSED_SHELL('',(#2574,#2575,#2576,#2577,#2578,#2579,#2580,#2581));
#3093=AXIS2_PLACEMENT_3D('',#4601,#3731,#3732);
#3094=AXIS2_PLACEMENT_3D('',#4602,#3733,#3734);
#3095=AXIS2_PLACEMENT_3D('',#4611,#3739,#3740);
#3096=AXIS2_PLACEMENT_3D('',#4617,#3744,#3745);
#3097=AXIS2_PLACEMENT_3D('',#4623,#3749,#3750);
#3098=AXIS2_PLACEMENT_3D('',#4629,#3754,#3755);
#3099=AXIS2_PLACEMENT_3D('',#4635,#3759,#3760);
#3100=AXIS2_PLACEMENT_3D('',#4638,#3763,#3764);
#3101=AXIS2_PLACEMENT_3D('',#4639,#3765,#3766);
#3102=AXIS2_PLACEMENT_3D('',#4640,#3767,#3768);
#3103=AXIS2_PLACEMENT_3D('',#4642,#3769,#3770);
#3104=AXIS2_PLACEMENT_3D('',#4643,#3771,#3772);
#3105=AXIS2_PLACEMENT_3D('',#4645,#3773,#3774);
#3106=AXIS2_PLACEMENT_3D('',#4646,#3775,#3776);
#3107=AXIS2_PLACEMENT_3D('',#4648,#3777,#3778);
#3108=AXIS2_PLACEMENT_3D('',#4650,#3780,#3781);
#3109=AXIS2_PLACEMENT_3D('',#4652,#3782,#3783);
#3110=AXIS2_PLACEMENT_3D('',#4654,#3785,#3786);
#3111=AXIS2_PLACEMENT_3D('',#4656,#3787,#3788);
#3112=AXIS2_PLACEMENT_3D('',#4658,#3790,#3791);
#3113=AXIS2_PLACEMENT_3D('',#4660,#3792,#3793);
#3114=AXIS2_PLACEMENT_3D('',#4661,#3794,#3795);
#3115=AXIS2_PLACEMENT_3D('',#4663,#3796,#3797);
#3116=AXIS2_PLACEMENT_3D('',#4665,#3799,#3800);
#3731=DIRECTION('axis',(0.,0.,1.));
#3732=DIRECTION('refdir',(1.,0.,0.));
#3733=DIRECTION('center_axis',(0.866025403784439,0.,-0.5));
#3734=DIRECTION('ref_axis',(0.5,0.,0.866025403784439));
#3735=DIRECTION('',(-0.5,0.,-0.866025403784439));
#3736=DIRECTION('',(0.,-1.,0.));
#3737=DIRECTION('',(0.5,0.,0.866025403784439));
#3738=DIRECTION('',(0.,-1.,0.));
#3739=DIRECTION('center_axis',(1.60246890531964E-16,0.,-1.));
#3740=DIRECTION('ref_axis',(1.,0.,1.60246890531964E-16));
#3741=DIRECTION('',(-1.,0.,-1.60246890531964E-16));
#3742=DIRECTION('',(0.,-1.,0.));
#3743=DIRECTION('',(1.,0.,1.60246890531964E-16));
#3744=DIRECTION('center_axis',(-0.866025403784439,0.,-0.5));
#3745=DIRECTION('ref_axis',(0.5,0.,-0.866025403784439));
#3746=DIRECTION('',(-0.5,0.,0.866025403784439));
#3747=DIRECTION('',(0.,-1.,0.));
#3748=DIRECTION('',(0.5,0.,-0.866025403784439));
#3749=DIRECTION('center_axis',(-0.866025403784439,0.,0.5));
#3750=DIRECTION('ref_axis',(-0.5,0.,-0.866025403784439));
#3751=DIRECTION('',(0.5,0.,0.866025403784439));
#3752=DIRECTION('',(0.,-1.,0.));
#3753=DIRECTION('',(-0.5,0.,-0.866025403784439));
#3754=DIRECTION('center_axis',(-1.60246890531964E-16,0.,1.));
#3755=DIRECTION('ref_axis',(-1.,0.,-1.60246890531964E-16));
#3756=DIRECTION('',(1.,0.,1.60246890531964E-16));
#3757=DIRECTION('',(0.,-1.,0.));
#3758=DIRECTION('',(-1.,0.,-1.60246890531964E-16));
#3759=DIRECTION('center_axis',(0.866025403784439,0.,0.5));
#3760=DIRECTION('ref_axis',(-0.5,0.,0.866025403784439));
#3761=DIRECTION('',(0.5,0.,-0.866025403784439));
#3762=DIRECTION('',(-0.5,0.,0.866025403784439));
#3763=DIRECTION('center_axis',(0.,1.,0.));
#3764=DIRECTION('ref_axis',(1.,0.,0.));
#3765=DIRECTION('center_axis',(0.,-1.,0.));
#3766=DIRECTION('ref_axis',(0.,0.,-1.));
#3767=DIRECTION('center_axis',(0.,1.,0.));
#3768=DIRECTION('ref_axis',(1.,0.,0.));
#3769=DIRECTION('center_axis',(0.,1.,0.));
#3770=DIRECTION('ref_axis',(1.,0.,0.));
#3771=DIRECTION('center_axis',(0.,1.,0.));
#3772=DIRECTION('ref_axis',(0.,0.,1.));
#3773=DIRECTION('center_axis',(0.,-1.,0.));
#3774=DIRECTION('ref_axis',(1.,0.,0.));
#3775=DIRECTION('center_axis',(0.,-1.,0.));
#3776=DIRECTION('ref_axis',(1.,0.,0.));
#3777=DIRECTION('center_axis',(0.,-1.,0.));
#3778=DIRECTION('ref_axis',(1.,0.,0.));
#3779=DIRECTION('',(0.707106781186547,0.707106781186548,8.65956056235493E-17));
#3780=DIRECTION('center_axis',(0.,-1.,0.));
#3781=DIRECTION('ref_axis',(1.,0.,0.));
#3782=DIRECTION('center_axis',(0.,-1.,0.));
#3783=DIRECTION('ref_axis',(1.,0.,0.));
#3784=DIRECTION('',(0.,1.,0.));
#3785=DIRECTION('center_axis',(0.,1.,0.));
#3786=DIRECTION('ref_axis',(1.,0.,0.));
#3787=DIRECTION('center_axis',(0.,-1.,0.));
#3788=DIRECTION('ref_axis',(1.,0.,0.));
#3789=DIRECTION('',(-0.707106781186547,0.707106781186548,-8.65956056235493E-17));
#3790=DIRECTION('center_axis',(0.,-1.,0.));
#3791=DIRECTION('ref_axis',(0.,0.,-1.));
#3792=DIRECTION('center_axis',(0.,-1.,0.));
#3793=DIRECTION('ref_axis',(1.,0.,0.));
#3794=DIRECTION('center_axis',(0.,1.,0.));
#3795=DIRECTION('ref_axis',(1.,0.,0.));
#3796=DIRECTION('center_axis',(0.,1.,0.));
#3797=DIRECTION('ref_axis',(1.,0.,0.));
#3798=DIRECTION('',(-0.447213595499958,0.894427190999916,-5.47678698264203E-17));
#3799=DIRECTION('center_axis',(0.,-1.,0.));
#3800=DIRECTION('ref_axis',(1.,0.,0.));
#3801=DIRECTION('',(0.,1.,0.));
#4601=CARTESIAN_POINT('',(0.,0.,0.));
#4602=CARTESIAN_POINT('Origin',(0.0866025403784439,-0.4,-0.15));
#4603=CARTESIAN_POINT('',(0.173205080756888,-0.4,0.));
#4604=CARTESIAN_POINT('',(0.0866025403784439,-0.4,-0.15));
#4605=CARTESIAN_POINT('',(0.173205080756888,-0.4,0.));
#4606=CARTESIAN_POINT('',(0.0866025403784439,-0.64,-0.15));
#4607=CARTESIAN_POINT('',(0.0866025403784439,-0.4,-0.15));
#4608=CARTESIAN_POINT('',(0.173205080756888,-0.64,0.));
#4609=CARTESIAN_POINT('',(0.173205080756888,-0.64,0.));
#4610=CARTESIAN_POINT('',(0.173205080756888,-0.4,0.));
#4611=CARTESIAN_POINT('Origin',(-0.0866025403784438,-0.4,-0.15));
#4612=CARTESIAN_POINT('',(-0.0866025403784438,-0.4,-0.15));
#4613=CARTESIAN_POINT('',(0.0866025403784439,-0.4,-0.15));
#4614=CARTESIAN_POINT('',(-0.0866025403784438,-0.64,-0.15));
#4615=CARTESIAN_POINT('',(-0.0866025403784438,-0.4,-0.15));
#4616=CARTESIAN_POINT('',(0.0866025403784439,-0.64,-0.15));
#4617=CARTESIAN_POINT('Origin',(-0.173205080756888,-0.4,-2.77555756156289E-17));
#4618=CARTESIAN_POINT('',(-0.173205080756888,-0.4,-2.12115047744981E-17));
#4619=CARTESIAN_POINT('',(-0.0866025403784438,-0.4,-0.15));
#4620=CARTESIAN_POINT('',(-0.173205080756888,-0.64,-2.77555756156289E-17));
#4621=CARTESIAN_POINT('',(-0.173205080756888,-0.4,-2.12115047744981E-17));
#4622=CARTESIAN_POINT('',(-0.0866025403784438,-0.64,-0.15));
#4623=CARTESIAN_POINT('Origin',(-0.0866025403784439,-0.4,0.15));
#4624=CARTESIAN_POINT('',(-0.0866025403784439,-0.4,0.15));
#4625=CARTESIAN_POINT('',(-0.173205080756888,-0.4,-2.12115047744981E-17));
#4626=CARTESIAN_POINT('',(-0.0866025403784439,-0.64,0.15));
#4627=CARTESIAN_POINT('',(-0.0866025403784439,-0.4,0.15));
#4628=CARTESIAN_POINT('',(-0.173205080756888,-0.64,-2.12115047744981E-17));
#4629=CARTESIAN_POINT('Origin',(0.0866025403784439,-0.4,0.15));
#4630=CARTESIAN_POINT('',(0.0866025403784439,-0.4,0.15));
#4631=CARTESIAN_POINT('',(-0.0866025403784439,-0.4,0.15));
#4632=CARTESIAN_POINT('',(0.0866025403784439,-0.64,0.15));
#4633=CARTESIAN_POINT('',(0.0866025403784439,-0.4,0.15));
#4634=CARTESIAN_POINT('',(-0.0866025403784439,-0.64,0.15));
#4635=CARTESIAN_POINT('Origin',(0.173205080756888,-0.4,0.));
#4636=CARTESIAN_POINT('',(0.0866025403784439,-0.4,0.15));
#4637=CARTESIAN_POINT('',(0.0866025403784439,-0.64,0.15));
#4638=CARTESIAN_POINT('Origin',(0.,-0.4,-2.77555756156289E-17));
#4639=CARTESIAN_POINT('Origin',(0.,-0.64,-2.77555756156289E-17));
#4640=CARTESIAN_POINT('Origin',(0.,-1.,0.));
#4641=CARTESIAN_POINT('',(-0.1954,-1.,2.39295984553393E-17));
#4642=CARTESIAN_POINT('Origin',(0.,-1.,0.));
#4643=CARTESIAN_POINT('Origin',(0.3,0.4,0.));
#4644=CARTESIAN_POINT('',(-0.3,0.4,-3.67394039744206E-17));
#4645=CARTESIAN_POINT('Origin',(0.,0.4,0.));
#4646=CARTESIAN_POINT('Origin',(0.,0.375,0.));
#4647=CARTESIAN_POINT('',(-0.35,0.35,-4.28626379701573E-17));
#4648=CARTESIAN_POINT('Origin',(0.,0.35,0.));
#4649=CARTESIAN_POINT('',(-0.325,0.375,-3.9801020972289E-17));
#4650=CARTESIAN_POINT('Origin',(0.,0.19,0.));
#4651=CARTESIAN_POINT('',(-0.35,0.03,-4.28626379701574E-17));
#4652=CARTESIAN_POINT('Origin',(0.,0.03,0.));
#4653=CARTESIAN_POINT('',(-0.35,0.19,-4.28626379701574E-17));
#4654=CARTESIAN_POINT('Origin',(0.,0.0149999999999999,0.));
#4655=CARTESIAN_POINT('',(-0.32,-3.29597460435593E-17,-3.91886975727153E-17));
#4656=CARTESIAN_POINT('Origin',(0.,0.,0.));
#4657=CARTESIAN_POINT('',(-0.335,0.0149999999999999,-4.10256677714363E-17));
#4658=CARTESIAN_POINT('Origin',(0.22,0.,0.));
#4659=CARTESIAN_POINT('',(-0.22,-6.93889390390723E-18,-2.69422295812418E-17));
#4660=CARTESIAN_POINT('Origin',(0.,0.,0.));
#4661=CARTESIAN_POINT('Origin',(0.,-0.02,0.));
#4662=CARTESIAN_POINT('',(-0.1954,-0.0492,2.39295984553393E-17));
#4663=CARTESIAN_POINT('Origin',(0.,-0.0492,0.));
#4664=CARTESIAN_POINT('',(-0.21,-0.02,-2.57175827820944E-17));
#4665=CARTESIAN_POINT('Origin',(0.,-0.8,0.));
#4666=CARTESIAN_POINT('',(-0.1954,-0.8,-2.39295984553393E-17));
#5346=UNCERTAINTY_MEASURE_WITH_UNIT(LENGTH_MEASURE(0.001),#5386,
'DISTANCE_ACCURACY_VALUE',
'Maximum model space distance between geometric entities at asserted c
onnectivities');
#5357=UNCERTAINTY_MEASURE_WITH_UNIT(LENGTH_MEASURE(0.001),#5386,
'DISTANCE_ACCURACY_VALUE',
'Maximum model space distance between geometric entities at asserted c
onnectivities');
#5374=(
GEOMETRIC_REPRESENTATION_CONTEXT(3)
GLOBAL_UNCERTAINTY_ASSIGNED_CONTEXT((#5346))
GLOBAL_UNIT_ASSIGNED_CONTEXT((#5386,#5388,#5389))
REPRESENTATION_CONTEXT('','3D')
);
#5385=(
GEOMETRIC_REPRESENTATION_CONTEXT(3)
GLOBAL_UNCERTAINTY_ASSIGNED_CONTEXT((#5357))
GLOBAL_UNIT_ASSIGNED_CONTEXT((#5386,#5388,#5389))
REPRESENTATION_CONTEXT('','3D')
);
#5386=(
LENGTH_UNIT()
NAMED_UNIT(*)
SI_UNIT(.CENTI.,.METRE.)
);
#5388=(
NAMED_UNIT(*)
PLANE_ANGLE_UNIT()
SI_UNIT($,.RADIAN.)
);
#5389=(
NAMED_UNIT(*)
SI_UNIT($,.STERADIAN.)
SOLID_ANGLE_UNIT()
);
#5406=SHAPE_DEFINITION_REPRESENTATION(#5438,#5487);
#5438=PRODUCT_DEFINITION_SHAPE('',$,#5515);
#5487=SHAPE_REPRESENTATION('',(#3093),#5374);
#5498=PRODUCT_DEFINITION_CONTEXT('part definition',#5581,'design');
#5515=PRODUCT_DEFINITION('M4x10 Cap Screw','M4x10 Cap Screw',#5542,#5498);
#5542=PRODUCT_DEFINITION_FORMATION('',$,#5599);
#5581=APPLICATION_CONTEXT(
'Core Data for Automotive Mechanical Design Process');
#5582=PRODUCT_CONTEXT('part definition',#5581,'mechanical');
#5599=PRODUCT('M4x10 Cap Screw','M4x10 Cap Screw','M4x10 Cap Screw',(#5582));
#5673=COLOUR_RGB('Black',0.12,0.14,0.17);
#5674=FILL_AREA_STYLE_COLOUR('',#5673);
#5675=FILL_AREA_STYLE('',(#5674));
#5676=SURFACE_STYLE_FILL_AREA(#5675);
#5677=SURFACE_SIDE_STYLE('',(#5676));
#5678=SURFACE_STYLE_USAGE(.BOTH.,#5677);
#5679=PRESENTATION_STYLE_ASSIGNMENT((#5678));
ENDSEC;
END-ISO-10303-21;
